ISO-10303-21;
HEADER;
FILE_DESCRIPTION (('STEP AP214'),
    '1' );
FILE_NAME ('Supporter 2.step',
    '2026-10-23T20:35:44',
    ( '' ),
    ( '' ),
    'SwSTEP 2.0',
    'SolidWorks 2025',
    '' );
FILE_SCHEMA (( 'AUTOMOTIVE_DESIGN' ));
ENDSEC;

DATA;
#21=ORIENTED_EDGE ( 'NONE', *, *, #1765, .T. ) ;
#43=DIRECTION ( 'NONE',  ( 1.000000000000000000, 0.000000000000000000, 0.000000000000000000 ) ) ;
#57=LENGTH_MEASURE_WITH_UNIT ( LENGTH_MEASURE( 0.02539999999999999897 ), #5956 );
#60=CARTESIAN_POINT ( 'NONE',  ( 0.000000000000000000, 1.496062992125984259, -0.2362204724409449341 ) ) ;
#64=DIRECTION ( 'NONE',  ( 0.000000000000000000, 1.000000000000000000, 0.000000000000000000 ) ) ;
#70=DIRECTION ( 'NONE',  ( -0.000000000000000000, -1.000000000000000000, -0.000000000000000000 ) ) ;
#99=EDGE_CURVE ( 'NONE', #6172, #3346, #1437, .T. ) ;
#105=FACE_BOUND ( 'NONE', #1838, .T. ) ;
#118=AXIS2_PLACEMENT_3D ( 'NONE', #1172, #3453, #43 ) ;
#130=CYLINDRICAL_SURFACE ( 'NONE', #5377, 0.2362204724409448231 ) ;
#144=EDGE_CURVE ( 'NONE', #1513, #5818, #3845, .T. ) ;
#161=VERTEX_POINT ( 'NONE', #540 ) ;
#162=CARTESIAN_POINT ( 'NONE',  ( 1.968503937007874072, 1.496062992125984259, 0.000000000000000000 ) ) ;
#167=DIRECTION ( 'NONE',  ( -0.000000000000000000, -1.000000000000000000, -0.000000000000000000 ) ) ;
#206=ORIENTED_EDGE ( 'NONE', *, *, #1251, .T. ) ;
#214=CARTESIAN_POINT ( 'NONE',  ( 1.968503937007874072, 0.000000000000000000, 0.000000000000000000 ) ) ;
#217=ORIENTED_EDGE ( 'NONE', *, *, #7387, .T. ) ;
#282=LINE ( 'NONE', #5487, #1734 ) ;
#286=APPLICATION_CONTEXT ( 'automotive_design' ) ;
#299=ADVANCED_FACE ( 'NONE', ( #2390, #602, #105 ), #1773, .T. ) ;
#302=UNCERTAINTY_MEASURE_WITH_UNIT (LENGTH_MEASURE( 1.000000000000000082E-05 ), #3871, 'distance_accuracy_value', 'NONE');
#332=ORIENTED_EDGE ( 'NONE', *, *, #2879, .T. ) ;
#367=EDGE_LOOP ( 'NONE', ( #1959, #4482 ) ) ;
#418=CARTESIAN_POINT ( 'NONE',  ( 0.000000000000000000, 0.000000000000000000, 0.000000000000000000 ) ) ;
#424=ORIENTED_EDGE ( 'NONE', *, *, #923, .T. ) ;
#465=DIRECTION ( 'NONE',  ( 0.000000000000000000, 1.000000000000000000, 0.000000000000000000 ) ) ;
#505=LINE ( 'NONE', #2311, #5123 ) ;
#535=AXIS2_PLACEMENT_3D ( 'NONE', #6664, #2000, #1481 ) ;
#539=DIRECTION ( 'NONE',  ( 0.000000000000000000, 0.000000000000000000, 1.000000000000000000 ) ) ;
#540=CARTESIAN_POINT ( 'NONE',  ( 0.000000000000000000, 1.496062992125984259, -0.4921259842519685179 ) ) ;
#572=ORIENTED_EDGE ( 'NONE', *, *, #2208, .F. ) ;
#575=ORIENTED_EDGE ( 'NONE', *, *, #144, .F. ) ;
#578=CARTESIAN_POINT ( 'NONE',  ( 1.968503937007874072, 0.000000000000000000, 0.4921259842519685179 ) ) ;
#602=FACE_OUTER_BOUND ( 'NONE', #6919, .T. ) ;
#603=EDGE_CURVE ( 'NONE', #4444, #2106, #3724, .T. ) ;
#625=PLANE ( 'NONE',  #7312 ) ;
#627=VECTOR ( 'NONE', #6886, 39.37007874015748143 ) ;
#634=EDGE_LOOP ( 'NONE', ( #920, #6744 ) ) ;
#637=CIRCLE ( 'NONE', #3324, 0.4921259842519685179 ) ;
#651=CARTESIAN_POINT ( 'NONE',  ( 1.968503937007874072, 0.000000000000000000, -0.2362204724409449619 ) ) ;
#689=DIRECTION ( 'NONE',  ( -0.000000000000000000, -1.000000000000000000, -0.000000000000000000 ) ) ;
#692=ORIENTED_EDGE ( 'NONE', *, *, #7245, .T. ) ;
#705=( GEOMETRIC_REPRESENTATION_CONTEXT ( 3 ) GLOBAL_UNCERTAINTY_ASSIGNED_CONTEXT ( ( #302 ) ) GLOBAL_UNIT_ASSIGNED_CONTEXT ( ( #3871, #7455, #7381 ) ) REPRESENTATION_CONTEXT ( 'NONE', 'WORKASPACE' ) );
#711=EDGE_CURVE ( 'NONE', #3346, #4166, #2412, .T. ) ;
#760=DIRECTION ( 'NONE',  ( 0.000000000000000000, 1.000000000000000000, 0.000000000000000000 ) ) ;
#780=ORIENTED_EDGE ( 'NONE', *, *, #4918, .T. ) ;
#829=DIRECTION ( 'NONE',  ( -1.000000000000000000, 0.000000000000000000, -0.000000000000000000 ) ) ;
#839=ORIENTED_EDGE ( 'NONE', *, *, #6725, .F. ) ;
#845=DIRECTION ( 'NONE',  ( 0.000000000000000000, 1.000000000000000000, 0.000000000000000000 ) ) ;
#850=DIRECTION ( 'NONE',  ( -1.000000000000000000, -0.000000000000000000, -0.000000000000000000 ) ) ;
#864=DIRECTION ( 'NONE',  ( 0.000000000000000000, 0.000000000000000000, 1.000000000000000000 ) ) ;
#867=AXIS2_PLACEMENT_3D ( 'NONE', #4206, #5973, #1163 ) ;
#869=LINE ( 'NONE', #6839, #2602 ) ;
#873=ORIENTED_EDGE ( 'NONE', *, *, #5995, .T. ) ;
#877=AXIS2_PLACEMENT_3D ( 'NONE', #2744, #465, #539 ) ;
#901=EDGE_LOOP ( 'NONE', ( #6061, #332, #5893, #4548 ) ) ;
#920=ORIENTED_EDGE ( 'NONE', *, *, #6725, .T. ) ;
#923=EDGE_CURVE ( 'NONE', #1513, #1261, #5686, .T. ) ;
#936=EDGE_CURVE ( 'NONE', #5718, #4898, #5884, .T. ) ;
#937=ADVANCED_FACE ( 'NONE', ( #2757 ), #4947, .T. ) ;
#958=AXIS2_PLACEMENT_3D ( 'NONE', #3708, #760, #2513 ) ;
#1001=ORIENTED_EDGE ( 'NONE', *, *, #4704, .F. ) ;
#1040=ADVANCED_FACE ( 'NONE', ( #6510, #6546, #3016 ), #1878, .F. ) ;
#1083=CIRCLE ( 'NONE', #3902, 0.2362204724409448231 ) ;
#1110=ADVANCED_FACE ( 'NONE', ( #1952 ), #5444, .F. ) ;
#1129=DIRECTION ( 'NONE',  ( 0.000000000000000000, 0.000000000000000000, -1.000000000000000000 ) ) ;
#1161=ORIENTED_EDGE ( 'NONE', *, *, #99, .T. ) ;
#1163=DIRECTION ( 'NONE',  ( 0.000000000000000000, 0.000000000000000000, 1.000000000000000000 ) ) ;
#1172=CARTESIAN_POINT ( 'NONE',  ( 0.9842519685039370358, 0.7480314960629921295, 0.000000000000000000 ) ) ;
#1179=ORIENTED_EDGE ( 'NONE', *, *, #4704, .T. ) ;
#1191=DIRECTION ( 'NONE',  ( 0.000000000000000000, 0.000000000000000000, -1.000000000000000000 ) ) ;
#1197=CARTESIAN_POINT ( 'NONE',  ( 1.968503937007874072, 1.496062992125984259, 0.000000000000000000 ) ) ;
#1205=CARTESIAN_POINT ( 'NONE',  ( 1.968503937007874072, 1.496062992125984259, -0.2362204724409449619 ) ) ;
#1217=DIRECTION ( 'NONE',  ( 1.000000000000000000, 0.000000000000000000, 0.000000000000000000 ) ) ;
#1251=EDGE_CURVE ( 'NONE', #5818, #4818, #869, .T. ) ;
#1261=VERTEX_POINT ( 'NONE', #7322 ) ;
#1325=EDGE_LOOP ( 'NONE', ( #6231, #4106 ) ) ;
#1326=CARTESIAN_POINT ( 'NONE',  ( 2.892866454678787531E-17, 1.496062992125984259, 0.2362204724409449341 ) ) ;
#1370=DIRECTION ( 'NONE',  ( -0.000000000000000000, -1.000000000000000000, -0.000000000000000000 ) ) ;
#1375=ORIENTED_EDGE ( 'NONE', *, *, #4398, .F. ) ;
#1386=LINE ( 'NONE', #5541, #6967 ) ;
#1404=CARTESIAN_POINT ( 'NONE',  ( 0.000000000000000000, 1.496062992125984259, 0.000000000000000000 ) ) ;
#1407=ORIENTED_EDGE ( 'NONE', *, *, #5673, .F. ) ;
#1414=ORIENTED_EDGE ( 'NONE', *, *, #1251, .F. ) ;
#1436=AXIS2_PLACEMENT_3D ( 'NONE', #4183, #2419, #4711 ) ;
#1437=LINE ( 'NONE', #2140, #5071 ) ;
#1444=CIRCLE ( 'NONE', #6462, 0.2362204724409449619 ) ;
#1481=DIRECTION ( 'NONE',  ( 0.000000000000000000, 0.000000000000000000, -1.000000000000000000 ) ) ;
#1495=ORIENTED_EDGE ( 'NONE', *, *, #144, .T. ) ;
#1509=CARTESIAN_POINT ( 'NONE',  ( 2.892866454678787531E-17, 0.000000000000000000, 0.2362204724409449341 ) ) ;
#1513=VERTEX_POINT ( 'NONE', #60 ) ;
#1525=ADVANCED_FACE ( 'NONE', ( #4721 ), #7053, .F. ) ;
#1531=VERTEX_POINT ( 'NONE', #3076 ) ;
#1539=DIRECTION ( 'NONE',  ( 0.000000000000000000, 0.000000000000000000, 1.000000000000000000 ) ) ;
#1556=CIRCLE ( 'NONE', #4730, 0.2362204724409448231 ) ;
#1573=ORIENTED_EDGE ( 'NONE', *, *, #603, .T. ) ;
#1586=DIRECTION ( 'NONE',  ( 0.000000000000000000, 0.000000000000000000, 1.000000000000000000 ) ) ;
#1594=CIRCLE ( 'NONE', #867, 0.2362204724409449341 ) ;
#1641=CARTESIAN_POINT ( 'NONE',  ( 0.000000000000000000, 0.000000000000000000, -0.4921259842519685179 ) ) ;
#1647=ORIENTED_EDGE ( 'NONE', *, *, #603, .F. ) ;
#1701=DIRECTION ( 'NONE',  ( 0.000000000000000000, 1.000000000000000000, 0.000000000000000000 ) ) ;
#1717=EDGE_LOOP ( 'NONE', ( #3998, #4981, #7337, #692 ) ) ;
#1721=VECTOR ( 'NONE', #7379, 39.37007874015748143 ) ;
#1734=VECTOR ( 'NONE', #850, 39.37007874015748143 ) ;
#1765=EDGE_CURVE ( 'NONE', #1531, #4444, #4409, .T. ) ;
#1773=PLANE ( 'NONE',  #7130 ) ;
#1778=DIRECTION ( 'NONE',  ( 1.000000000000000000, 0.000000000000000000, 0.000000000000000000 ) ) ;
#1783=EDGE_LOOP ( 'NONE', ( #1414, #6772, #424, #572 ) ) ;
#1807=DIRECTION ( 'NONE',  ( -0.000000000000000000, -1.000000000000000000, -0.000000000000000000 ) ) ;
#1809=ADVANCED_FACE ( 'NONE', ( #6857 ), #6816, .T. ) ;
#1838=EDGE_LOOP ( 'NONE', ( #6235, #7309 ) ) ;
#1864=DIRECTION ( 'NONE',  ( 0.000000000000000000, 1.000000000000000000, 0.000000000000000000 ) ) ;
#1878=PLANE ( 'NONE',  #6498 ) ;
#1925=CARTESIAN_POINT ( 'NONE',  ( 0.000000000000000000, 0.000000000000000000, 0.4921259842519685179 ) ) ;
#1952=FACE_OUTER_BOUND ( 'NONE', #2722, .T. ) ;
#1959=ORIENTED_EDGE ( 'NONE', *, *, #936, .T. ) ;
#1990=CARTESIAN_POINT ( 'NONE',  ( 0.000000000000000000, 1.496062992125984259, 0.4921259842519685179 ) ) ;
#2000=DIRECTION ( 'NONE',  ( -0.000000000000000000, -1.000000000000000000, -0.000000000000000000 ) ) ;
#2016=AXIS2_PLACEMENT_3D ( 'NONE', #2371, #5287, #1217 ) ;
#2032=DIRECTION ( 'NONE',  ( 0.000000000000000000, 0.000000000000000000, 1.000000000000000000 ) ) ;
#2106=VERTEX_POINT ( 'NONE', #3086 ) ;
#2134=DIRECTION ( 'NONE',  ( 0.000000000000000000, 0.000000000000000000, 1.000000000000000000 ) ) ;
#2135=DIRECTION ( 'NONE',  ( -0.000000000000000000, -1.000000000000000000, -0.000000000000000000 ) ) ;
#2140=CARTESIAN_POINT ( 'NONE',  ( 0.000000000000000000, 1.496062992125984259, 0.4921259842519685179 ) ) ;
#2150=DIRECTION ( 'NONE',  ( 0.000000000000000000, 0.000000000000000000, 1.000000000000000000 ) ) ;
#2157=ORIENTED_EDGE ( 'NONE', *, *, #5684, .T. ) ;
#2183=DIMENSIONAL_EXPONENTS ( 1.000000000000000000, 0.000000000000000000, 0.000000000000000000, 0.000000000000000000, 0.000000000000000000, 0.000000000000000000, 0.000000000000000000 ) ;
#2208=EDGE_CURVE ( 'NONE', #4818, #1261, #4624, .T. ) ;
#2225=AXIS2_PLACEMENT_3D ( 'NONE', #5000, #2739, #1586 ) ;
#2264=LENGTH_MEASURE_WITH_UNIT ( LENGTH_MEASURE( 0.02539999999999999897 ), #5688 );
#2311=CARTESIAN_POINT ( 'NONE',  ( 1.220472440944881942, 0.7480314960629921295, 0.000000000000000000 ) ) ;
#2339=LINE ( 'NONE', #2945, #2638 ) ;
#2361=ORIENTED_EDGE ( 'NONE', *, *, #4918, .F. ) ;
#2371=CARTESIAN_POINT ( 'NONE',  ( 0.9842519685039370358, 0.7480314960629921295, 0.4921259842519685179 ) ) ;
#2384=PRODUCT ( 'Supporter 2', 'Supporter 2', '', ( #2714 ) ) ;
#2390=FACE_BOUND ( 'NONE', #3141, .T. ) ;
#2404=STYLED_ITEM('',(#7573),#4080);
#2412=LINE ( 'NONE', #1925, #5401 ) ;
#2419=DIRECTION ( 'NONE',  ( 0.000000000000000000, 1.000000000000000000, 0.000000000000000000 ) ) ;
#2446=CARTESIAN_POINT ( 'NONE',  ( 0.000000000000000000, 0.000000000000000000, 0.000000000000000000 ) ) ;
#2451=ORIENTED_EDGE ( 'NONE', *, *, #5808, .T. ) ;
#2471=FACE_BOUND ( 'NONE', #5070, .T. ) ;
#2488=CYLINDRICAL_SURFACE ( 'NONE', #5051, 0.2362204724409449619 ) ;
#2513=DIRECTION ( 'NONE',  ( 0.000000000000000000, 0.000000000000000000, 1.000000000000000000 ) ) ;
#2516=EDGE_LOOP ( 'NONE', ( #6555, #4916, #3101, #5284 ) ) ;
#2525=EDGE_CURVE ( 'NONE', #1531, #2899, #1083, .T. ) ;
#2539=EDGE_LOOP ( 'NONE', ( #217, #4517, #2361, #7258 ) ) ;
#2551=CARTESIAN_POINT ( 'NONE',  ( 0.9842519685039370358, 0.7480314960629921295, 0.000000000000000000 ) ) ;
#2553=ORIENTED_EDGE ( 'NONE', *, *, #2664, .F. ) ;
#2581=PRODUCT_DEFINITION_SHAPE ( 'NONE', 'NONE',  #2700 ) ;
#2585=AXIS2_PLACEMENT_3D ( 'NONE', #6099, #2643, #2150 ) ;
#2602=VECTOR ( 'NONE', #2135, 39.37007874015748143 ) ;
#2609=ORIENTED_EDGE ( 'NONE', *, *, #3704, .F. ) ;
#2638=VECTOR ( 'NONE', #5288, 39.37007874015748143 ) ;
#2643=DIRECTION ( 'NONE',  ( 0.000000000000000000, 1.000000000000000000, 0.000000000000000000 ) ) ;
#2651=CIRCLE ( 'NONE', #5107, 0.4921259842519685179 ) ;
#2664=EDGE_CURVE ( 'NONE', #2899, #2106, #505, .T. ) ;
#2700=PRODUCT_DEFINITION ( 'UNKNOWN', '', #3495, #4194 ) ;
#2714=PRODUCT_CONTEXT ( 'NONE', #286, 'mechanical' ) ;
#2722=EDGE_LOOP ( 'NONE', ( #1495, #206, #839, #6680 ) ) ;
#2725=CARTESIAN_POINT ( 'NONE',  ( 0.000000000000000000, 1.496062992125984259, -0.2362204724409449341 ) ) ;
#2730=ORIENTED_EDGE ( 'NONE', *, *, #2664, .T. ) ;
#2736=LINE ( 'NONE', #3266, #5011 ) ;
#2739=DIRECTION ( 'NONE',  ( 0.000000000000000000, 1.000000000000000000, 0.000000000000000000 ) ) ;
#2741=DIRECTION ( 'NONE',  ( 1.000000000000000000, 0.000000000000000000, 0.000000000000000000 ) ) ;
#2744=CARTESIAN_POINT ( 'NONE',  ( 1.968503937007874072, 1.496062992125984259, 0.000000000000000000 ) ) ;
#2757=FACE_OUTER_BOUND ( 'NONE', #1325, .T. ) ;
#2819=AXIS2_PLACEMENT_3D ( 'NONE', #5842, #3506, #7136 ) ;
#2860=EDGE_LOOP ( 'NONE', ( #873, #2157, #5250, #1407 ) ) ;
#2879=EDGE_CURVE ( 'NONE', #4791, #5757, #1444, .T. ) ;
#2890=CARTESIAN_POINT ( 'NONE',  ( 1.968503937007874072, 1.496062992125984259, 0.2362204724409449619 ) ) ;
#2899=VERTEX_POINT ( 'NONE', #7021 ) ;
#2910=AXIS2_PLACEMENT_3D ( 'NONE', #4179, #3927, #1539 ) ;
#2925=ORIENTED_EDGE ( 'NONE', *, *, #1765, .F. ) ;
#2945=CARTESIAN_POINT ( 'NONE',  ( 0.000000000000000000, 1.496062992125984259, -0.4921259842519685179 ) ) ;
#2947=CARTESIAN_POINT ( 'NONE',  ( 0.9842519685039370358, 0.7480314960629921295, 0.000000000000000000 ) ) ;
#2956=AXIS2_PLACEMENT_3D ( 'NONE', #3662, #6076, #829 ) ;
#2971=CLOSED_SHELL ( 'NONE', ( #3892, #5725, #1110, #299, #1040, #1809, #6233, #4217, #3273, #1525, #5489, #3220, #937 ) ) ;
#2979=CYLINDRICAL_SURFACE ( 'NONE', #3389, 0.4921259842519685179 ) ;
#3016=FACE_BOUND ( 'NONE', #367, .T. ) ;
#3062=CARTESIAN_POINT ( 'NONE',  ( 0.000000000000000000, 1.496062992125984259, -0.4921259842519685179 ) ) ;
#3076=CARTESIAN_POINT ( 'NONE',  ( 0.7480314960629922405, 0.7480314960629921295, 0.000000000000000000 ) ) ;
#3086=CARTESIAN_POINT ( 'NONE',  ( 1.220472440944881942, 0.7480314960629921295, 0.4921259842519685179 ) ) ;
#3098=DIRECTION ( 'NONE',  ( 1.000000000000000000, 0.000000000000000000, 0.000000000000000000 ) ) ;
#3101=ORIENTED_EDGE ( 'NONE', *, *, #3991, .F. ) ;
#3141=EDGE_LOOP ( 'NONE', ( #575, #6671 ) ) ;
#3156=CARTESIAN_POINT ( 'NONE',  ( 0.9842519685039370358, 0.7480314960629921295, 0.000000000000000000 ) ) ;
#3185=DIRECTION ( 'NONE',  ( 0.000000000000000000, 0.000000000000000000, 1.000000000000000000 ) ) ;
#3192=DIRECTION ( 'NONE',  ( -1.000000000000000000, -0.000000000000000000, -0.000000000000000000 ) ) ;
#3199=CARTESIAN_POINT ( 'NONE',  ( 0.000000000000000000, 1.496062992125984259, 0.4921259842519685179 ) ) ;
#3220=ADVANCED_FACE ( 'NONE', ( #6426 ), #4634, .F. ) ;
#3234=DIRECTION ( 'NONE',  ( -0.000000000000000000, -1.000000000000000000, -0.000000000000000000 ) ) ;
#3266=CARTESIAN_POINT ( 'NONE',  ( 1.968503937007874072, 1.496062992125984259, 0.4921259842519685179 ) ) ;
#3273=ADVANCED_FACE ( 'NONE', ( #5414 ), #625, .F. ) ;
#3280=EDGE_CURVE ( 'NONE', #161, #4527, #2339, .T. ) ;
#3294=AXIS2_PLACEMENT_3D ( 'NONE', #3156, #864, #6148 ) ;
#3307=CARTESIAN_POINT ( 'NONE',  ( 0.000000000000000000, 0.000000000000000000, 0.4921259842519685179 ) ) ;
#3324=AXIS2_PLACEMENT_3D ( 'NONE', #6487, #1701, #3469 ) ;
#3329=EDGE_CURVE ( 'NONE', #5818, #1513, #5245, .T. ) ;
#3346=VERTEX_POINT ( 'NONE', #3307 ) ;
#3370=EDGE_CURVE ( 'NONE', #4133, #4166, #2736, .T. ) ;
#3389=AXIS2_PLACEMENT_3D ( 'NONE', #4170, #5277, #6390 ) ;
#3395=CIRCLE ( 'NONE', #958, 0.4921259842519685179 ) ;
#3418=ORIENTED_EDGE ( 'NONE', *, *, #711, .T. ) ;
#3453=DIRECTION ( 'NONE',  ( -0.000000000000000000, -0.000000000000000000, 1.000000000000000000 ) ) ;
#3469=DIRECTION ( 'NONE',  ( 0.000000000000000000, 0.000000000000000000, 1.000000000000000000 ) ) ;
#3495=PRODUCT_DEFINITION_FORMATION_WITH_SPECIFIED_SOURCE ( 'ANY', '', #2384, .NOT_KNOWN. ) ;
#3506=DIRECTION ( 'NONE',  ( 0.000000000000000000, 1.000000000000000000, 0.000000000000000000 ) ) ;
#3556=DIRECTION ( 'NONE',  ( 0.000000000000000000, -0.000000000000000000, 1.000000000000000000 ) ) ;
#3561=AXIS2_PLACEMENT_3D ( 'NONE', #4368, #4982, #7300 ) ;
#3564=ORIENTED_EDGE ( 'NONE', *, *, #6639, .T. ) ;
#3633=MECHANICAL_DESIGN_GEOMETRIC_PRESENTATION_REPRESENTATION('',(#2404),#705);
#3662=CARTESIAN_POINT ( 'NONE',  ( 0.000000000000000000, 1.496062992125984259, 0.4921259842519685179 ) ) ;
#3704=EDGE_CURVE ( 'NONE', #2899, #1531, #4883, .T. ) ;
#3708=CARTESIAN_POINT ( 'NONE',  ( 1.968503937007874072, 1.496062992125984259, 0.000000000000000000 ) ) ;
#3724=CIRCLE ( 'NONE', #2016, 0.2362204724409448231 ) ;
#3821=CARTESIAN_POINT ( 'NONE',  ( 1.968503937007874072, 0.000000000000000000, 0.2362204724409449619 ) ) ;
#3845=CIRCLE ( 'NONE', #5917, 0.2362204724409449341 ) ;
#3871=( CONVERSION_BASED_UNIT ( 'INCH', #2264 ) LENGTH_UNIT ( ) NAMED_UNIT ( #2183 ) );
#3892=ADVANCED_FACE ( 'NONE', ( #5909 ), #130, .F. ) ;
#3902=AXIS2_PLACEMENT_3D ( 'NONE', #2551, #7024, #1778 ) ;
#3922=ORIENTED_EDGE ( 'NONE', *, *, #3370, .F. ) ;
#3927=DIRECTION ( 'NONE',  ( 0.000000000000000000, 1.000000000000000000, 0.000000000000000000 ) ) ;
#3991=EDGE_CURVE ( 'NONE', #4166, #7153, #2651, .T. ) ;
#3993=( NAMED_UNIT ( * ) PLANE_ANGLE_UNIT ( ) SI_UNIT ( $, .RADIAN. ) );
#3998=ORIENTED_EDGE ( 'NONE', *, *, #5476, .T. ) ;
#4039=APPLICATION_CONTEXT ( 'automotive_design' ) ;
#4078=DIRECTION ( 'NONE',  ( -0.000000000000000000, -0.000000000000000000, 1.000000000000000000 ) ) ;
#4080=MANIFOLD_SOLID_BREP ( 'Cut-Extrude1', #2971 ) ;
#4106=ORIENTED_EDGE ( 'NONE', *, *, #2525, .T. ) ;
#4107=( CONVERSION_BASED_UNIT ( 'INCH', #57 ) LENGTH_UNIT ( ) NAMED_UNIT ( #5848 ) );
#4133=VERTEX_POINT ( 'NONE', #6896 ) ;
#4166=VERTEX_POINT ( 'NONE', #578 ) ;
#4170=CARTESIAN_POINT ( 'NONE',  ( 1.968503937007874072, 1.496062992125984259, 0.000000000000000000 ) ) ;
#4173=( GEOMETRIC_REPRESENTATION_CONTEXT ( 3 ) GLOBAL_UNCERTAINTY_ASSIGNED_CONTEXT ( ( #6042 ) ) GLOBAL_UNIT_ASSIGNED_CONTEXT ( ( #4107, #3993, #6943 ) ) REPRESENTATION_CONTEXT ( 'NONE', 'WORKASPACE' ) );
#4179=CARTESIAN_POINT ( 'NONE',  ( 0.000000000000000000, 1.496062992125984259, 0.000000000000000000 ) ) ;
#4183=CARTESIAN_POINT ( 'NONE',  ( 0.000000000000000000, 0.000000000000000000, 0.000000000000000000 ) ) ;
#4194=PRODUCT_DEFINITION_CONTEXT ( 'detailed design', #4039, 'design' ) ;
#4206=CARTESIAN_POINT ( 'NONE',  ( 0.000000000000000000, 0.000000000000000000, 0.000000000000000000 ) ) ;
#4209=ORIENTED_EDGE ( 'NONE', *, *, #2525, .F. ) ;
#4217=ADVANCED_FACE ( 'NONE', ( #6463 ), #2979, .T. ) ;
#4269=FACE_OUTER_BOUND ( 'NONE', #5678, .T. ) ;
#4368=CARTESIAN_POINT ( 'NONE',  ( 0.9842519685039370358, 0.7480314960629921295, 0.000000000000000000 ) ) ;
#4398=EDGE_CURVE ( 'NONE', #2106, #4444, #1556, .T. ) ;
#4404=CYLINDRICAL_SURFACE ( 'NONE', #535, 0.2362204724409449619 ) ;
#4409=LINE ( 'NONE', #5569, #6452 ) ;
#4444=VERTEX_POINT ( 'NONE', #4897 ) ;
#4482=ORIENTED_EDGE ( 'NONE', *, *, #6355, .T. ) ;
#4506=AXIS2_PLACEMENT_3D ( 'NONE', #6208, #70, #5721 ) ;
#4517=ORIENTED_EDGE ( 'NONE', *, *, #99, .F. ) ;
#4527=VERTEX_POINT ( 'NONE', #1641 ) ;
#4548=ORIENTED_EDGE ( 'NONE', *, *, #6355, .F. ) ;
#4561=CIRCLE ( 'NONE', #877, 0.2362204724409449619 ) ;
#4587=CARTESIAN_POINT ( 'NONE',  ( 1.968503937007874072, 1.496062992125984259, -0.4921259842519685179 ) ) ;
#4624=CIRCLE ( 'NONE', #1436, 0.2362204724409449341 ) ;
#4634=CYLINDRICAL_SURFACE ( 'NONE', #118, 0.2362204724409448231 ) ;
#4655=LINE ( 'NONE', #4735, #6382 ) ;
#4671=VECTOR ( 'NONE', #5475, 39.37007874015748143 ) ;
#4704=EDGE_CURVE ( 'NONE', #4133, #7450, #3395, .T. ) ;
#4711=DIRECTION ( 'NONE',  ( 0.000000000000000000, 0.000000000000000000, 1.000000000000000000 ) ) ;
#4721=FACE_OUTER_BOUND ( 'NONE', #1783, .T. ) ;
#4730=AXIS2_PLACEMENT_3D ( 'NONE', #5485, #5446, #3098 ) ;
#4735=CARTESIAN_POINT ( 'NONE',  ( 1.968503937007874072, 1.496062992125984259, -0.2362204724409449619 ) ) ;
#4779=LINE ( 'NONE', #2890, #7117 ) ;
#4791=VERTEX_POINT ( 'NONE', #6761 ) ;
#4792=EDGE_LOOP ( 'NONE', ( #5955, #5598, #1001, #5480 ) ) ;
#4795=DIRECTION ( 'NONE',  ( 1.000000000000000000, 0.000000000000000000, -0.000000000000000000 ) ) ;
#4807=PLANE ( 'NONE',  #2956 ) ;
#4810=DIRECTION ( 'NONE',  ( 0.000000000000000000, -0.000000000000000000, 1.000000000000000000 ) ) ;
#4818=VERTEX_POINT ( 'NONE', #1509 ) ;
#4831=SHAPE_DEFINITION_REPRESENTATION ( #2581, #5531 ) ;
#4883=CIRCLE ( 'NONE', #3294, 0.2362204724409448231 ) ;
#4897=CARTESIAN_POINT ( 'NONE',  ( 0.7480314960629922405, 0.7480314960629921295, 0.4921259842519685179 ) ) ;
#4898=VERTEX_POINT ( 'NONE', #3821 ) ;
#4916=ORIENTED_EDGE ( 'NONE', *, *, #5476, .F. ) ;
#4918=EDGE_CURVE ( 'NONE', #161, #6172, #637, .T. ) ;
#4947=PLANE ( 'NONE',  #3561 ) ;
#4981=ORIENTED_EDGE ( 'NONE', *, *, #3280, .F. ) ;
#4982=DIRECTION ( 'NONE',  ( 0.000000000000000000, 0.000000000000000000, 1.000000000000000000 ) ) ;
#5000=CARTESIAN_POINT ( 'NONE',  ( 1.968503937007874072, 0.000000000000000000, 0.000000000000000000 ) ) ;
#5011=VECTOR ( 'NONE', #3234, 39.37007874015748143 ) ;
#5031=EDGE_LOOP ( 'NONE', ( #2925, #2609, #2730, #7458 ) ) ;
#5051=AXIS2_PLACEMENT_3D ( 'NONE', #162, #5236, #1129 ) ;
#5070=EDGE_LOOP ( 'NONE', ( #1375, #1647 ) ) ;
#5071=VECTOR ( 'NONE', #1370, 39.37007874015748143 ) ;
#5107=AXIS2_PLACEMENT_3D ( 'NONE', #214, #5533, #3185 ) ;
#5123=VECTOR ( 'NONE', #4078, 39.37007874015748143 ) ;
#5166=AXIS2_PLACEMENT_3D ( 'NONE', #418, #2134, #2741 ) ;
#5172=CARTESIAN_POINT ( 'NONE',  ( 1.968503937007874072, 0.000000000000000000, -0.4921259842519685179 ) ) ;
#5236=DIRECTION ( 'NONE',  ( -0.000000000000000000, -1.000000000000000000, -0.000000000000000000 ) ) ;
#5245=CIRCLE ( 'NONE', #2910, 0.2362204724409449341 ) ;
#5250=ORIENTED_EDGE ( 'NONE', *, *, #936, .F. ) ;
#5277=DIRECTION ( 'NONE',  ( -0.000000000000000000, -1.000000000000000000, -0.000000000000000000 ) ) ;
#5284=ORIENTED_EDGE ( 'NONE', *, *, #711, .F. ) ;
#5287=DIRECTION ( 'NONE',  ( 0.000000000000000000, 0.000000000000000000, 1.000000000000000000 ) ) ;
#5288=DIRECTION ( 'NONE',  ( -0.000000000000000000, -1.000000000000000000, -0.000000000000000000 ) ) ;
#5311=DIRECTION ( 'NONE',  ( -0.000000000000000000, -1.000000000000000000, -0.000000000000000000 ) ) ;
#5324=DIRECTION ( 'NONE',  ( 0.000000000000000000, 0.000000000000000000, 1.000000000000000000 ) ) ;
#5377=AXIS2_PLACEMENT_3D ( 'NONE', #2947, #6431, #5866 ) ;
#5397=FACE_OUTER_BOUND ( 'NONE', #2860, .T. ) ;
#5401=VECTOR ( 'NONE', #6589, 39.37007874015748143 ) ;
#5414=FACE_OUTER_BOUND ( 'NONE', #1717, .T. ) ;
#5422=CIRCLE ( 'NONE', #2225, 0.2362204724409449619 ) ;
#5444=CYLINDRICAL_SURFACE ( 'NONE', #7338, 0.2362204724409449341 ) ;
#5446=DIRECTION ( 'NONE',  ( 0.000000000000000000, 0.000000000000000000, 1.000000000000000000 ) ) ;
#5475=DIRECTION ( 'NONE',  ( 1.000000000000000000, 0.000000000000000000, 0.000000000000000000 ) ) ;
#5476=EDGE_CURVE ( 'NONE', #7153, #4527, #282, .T. ) ;
#5480=ORIENTED_EDGE ( 'NONE', *, *, #3370, .T. ) ;
#5485=CARTESIAN_POINT ( 'NONE',  ( 0.9842519685039370358, 0.7480314960629921295, 0.4921259842519685179 ) ) ;
#5487=CARTESIAN_POINT ( 'NONE',  ( 0.000000000000000000, 0.000000000000000000, -0.4921259842519685179 ) ) ;
#5489=ADVANCED_FACE ( 'NONE', ( #6699 ), #4404, .F. ) ;
#5508=CARTESIAN_POINT ( 'NONE',  ( 1.968503937007874072, 1.496062992125984259, -0.4921259842519685179 ) ) ;
#5531=SHAPE_REPRESENTATION ( 'Supporter 2', ( #5166 ), #4173 ) ;
#5533=DIRECTION ( 'NONE',  ( 0.000000000000000000, 1.000000000000000000, 0.000000000000000000 ) ) ;
#5541=CARTESIAN_POINT ( 'NONE',  ( 0.000000000000000000, 1.496062992125984259, -0.4921259842519685179 ) ) ;
#5569=CARTESIAN_POINT ( 'NONE',  ( 0.7480314960629922405, 0.7480314960629921295, 0.000000000000000000 ) ) ;
#5598=ORIENTED_EDGE ( 'NONE', *, *, #7245, .F. ) ;
#5673=EDGE_CURVE ( 'NONE', #5757, #5718, #4655, .T. ) ;
#5678=EDGE_LOOP ( 'NONE', ( #3418, #3922, #7187, #1161 ) ) ;
#5684=EDGE_CURVE ( 'NONE', #4791, #4898, #4779, .T. ) ;
#5686=LINE ( 'NONE', #2725, #1721 ) ;
#5688=( LENGTH_UNIT ( ) NAMED_UNIT ( * ) SI_UNIT ( $, .METRE. ) );
#5718=VERTEX_POINT ( 'NONE', #651 ) ;
#5721=DIRECTION ( 'NONE',  ( 0.000000000000000000, 0.000000000000000000, -1.000000000000000000 ) ) ;
#5725=ADVANCED_FACE ( 'NONE', ( #5397 ), #2488, .F. ) ;
#5757=VERTEX_POINT ( 'NONE', #1205 ) ;
#5808=EDGE_CURVE ( 'NONE', #6172, #4133, #6618, .T. ) ;
#5818=VERTEX_POINT ( 'NONE', #1326 ) ;
#5842=CARTESIAN_POINT ( 'NONE',  ( 0.000000000000000000, 0.000000000000000000, 0.000000000000000000 ) ) ;
#5848=DIMENSIONAL_EXPONENTS ( 1.000000000000000000, 0.000000000000000000, 0.000000000000000000, 0.000000000000000000, 0.000000000000000000, 0.000000000000000000, 0.000000000000000000 ) ;
#5866=DIRECTION ( 'NONE',  ( 1.000000000000000000, 0.000000000000000000, 0.000000000000000000 ) ) ;
#5884=CIRCLE ( 'NONE', #2585, 0.2362204724409449619 ) ;
#5893=ORIENTED_EDGE ( 'NONE', *, *, #5673, .T. ) ;
#5909=FACE_OUTER_BOUND ( 'NONE', #7382, .T. ) ;
#5914=AXIS2_PLACEMENT_3D ( 'NONE', #6568, #1807, #1191 ) ;
#5917=AXIS2_PLACEMENT_3D ( 'NONE', #1404, #845, #2032 ) ;
#5955=ORIENTED_EDGE ( 'NONE', *, *, #3991, .T. ) ;
#5956=( LENGTH_UNIT ( ) NAMED_UNIT ( * ) SI_UNIT ( $, .METRE. ) );
#5963=DIRECTION ( 'NONE',  ( 0.000000000000000000, 0.000000000000000000, 1.000000000000000000 ) ) ;
#5973=DIRECTION ( 'NONE',  ( 0.000000000000000000, 1.000000000000000000, 0.000000000000000000 ) ) ;
#5976=CARTESIAN_POINT ( 'NONE',  ( 0.000000000000000000, 1.496062992125984259, 0.000000000000000000 ) ) ;
#5995=EDGE_CURVE ( 'NONE', #5757, #4791, #4561, .T. ) ;
#6042=UNCERTAINTY_MEASURE_WITH_UNIT (LENGTH_MEASURE( 1.000000000000000082E-05 ), #4107, 'distance_accuracy_value', 'NONE');
#6059=DIRECTION ( 'NONE',  ( 0.000000000000000000, 1.000000000000000000, 0.000000000000000000 ) ) ;
#6061=ORIENTED_EDGE ( 'NONE', *, *, #5684, .F. ) ;
#6076=DIRECTION ( 'NONE',  ( 0.000000000000000000, 0.000000000000000000, -1.000000000000000000 ) ) ;
#6099=CARTESIAN_POINT ( 'NONE',  ( 1.968503937007874072, 0.000000000000000000, 0.000000000000000000 ) ) ;
#6127=CIRCLE ( 'NONE', #2819, 0.4921259842519685179 ) ;
#6148=DIRECTION ( 'NONE',  ( 1.000000000000000000, 0.000000000000000000, 0.000000000000000000 ) ) ;
#6172=VERTEX_POINT ( 'NONE', #3199 ) ;
#6208=CARTESIAN_POINT ( 'NONE',  ( 0.000000000000000000, 1.496062992125984259, 0.000000000000000000 ) ) ;
#6231=ORIENTED_EDGE ( 'NONE', *, *, #3704, .T. ) ;
#6233=ADVANCED_FACE ( 'NONE', ( #2471, #4269 ), #4807, .F. ) ;
#6235=ORIENTED_EDGE ( 'NONE', *, *, #5995, .F. ) ;
#6355=EDGE_CURVE ( 'NONE', #4898, #5718, #5422, .T. ) ;
#6382=VECTOR ( 'NONE', #689, 39.37007874015748143 ) ;
#6390=DIRECTION ( 'NONE',  ( 0.000000000000000000, 0.000000000000000000, -1.000000000000000000 ) ) ;
#6426=FACE_OUTER_BOUND ( 'NONE', #5031, .T. ) ;
#6431=DIRECTION ( 'NONE',  ( -0.000000000000000000, -0.000000000000000000, 1.000000000000000000 ) ) ;
#6452=VECTOR ( 'NONE', #7347, 39.37007874015748143 ) ;
#6462=AXIS2_PLACEMENT_3D ( 'NONE', #1197, #1864, #5963 ) ;
#6463=FACE_OUTER_BOUND ( 'NONE', #4792, .T. ) ;
#6487=CARTESIAN_POINT ( 'NONE',  ( 0.000000000000000000, 1.496062992125984259, 0.000000000000000000 ) ) ;
#6498=AXIS2_PLACEMENT_3D ( 'NONE', #2446, #6059, #3556 ) ;
#6510=FACE_OUTER_BOUND ( 'NONE', #2516, .T. ) ;
#6546=FACE_BOUND ( 'NONE', #634, .T. ) ;
#6555=ORIENTED_EDGE ( 'NONE', *, *, #7387, .F. ) ;
#6568=CARTESIAN_POINT ( 'NONE',  ( 0.000000000000000000, 1.496062992125984259, 0.000000000000000000 ) ) ;
#6589=DIRECTION ( 'NONE',  ( 1.000000000000000000, 0.000000000000000000, 0.000000000000000000 ) ) ;
#6618=LINE ( 'NONE', #1990, #4671 ) ;
#6639=EDGE_CURVE ( 'NONE', #7450, #161, #1386, .T. ) ;
#6664=CARTESIAN_POINT ( 'NONE',  ( 1.968503937007874072, 1.496062992125984259, 0.000000000000000000 ) ) ;
#6671=ORIENTED_EDGE ( 'NONE', *, *, #3329, .F. ) ;
#6680=ORIENTED_EDGE ( 'NONE', *, *, #923, .F. ) ;
#6699=FACE_OUTER_BOUND ( 'NONE', #901, .T. ) ;
#6725=EDGE_CURVE ( 'NONE', #1261, #4818, #1594, .T. ) ;
#6744=ORIENTED_EDGE ( 'NONE', *, *, #2208, .T. ) ;
#6761=CARTESIAN_POINT ( 'NONE',  ( 1.968503937007874072, 1.496062992125984259, 0.2362204724409449619 ) ) ;
#6772=ORIENTED_EDGE ( 'NONE', *, *, #3329, .T. ) ;
#6816=CYLINDRICAL_SURFACE ( 'NONE', #4506, 0.4921259842519685179 ) ;
#6839=CARTESIAN_POINT ( 'NONE',  ( 2.892866454678787531E-17, 1.496062992125984259, 0.2362204724409449341 ) ) ;
#6857=FACE_OUTER_BOUND ( 'NONE', #2539, .T. ) ;
#6873=ADVANCED_BREP_SHAPE_REPRESENTATION ( '', ( #4080, #5166 ), #4173 ) ;
#6886=DIRECTION ( 'NONE',  ( -0.000000000000000000, -1.000000000000000000, -0.000000000000000000 ) ) ;
#6896=CARTESIAN_POINT ( 'NONE',  ( 1.968503937007874072, 1.496062992125984259, 0.4921259842519685179 ) ) ;
#6919=EDGE_LOOP ( 'NONE', ( #780, #2451, #1179, #3564 ) ) ;
#6943=( NAMED_UNIT ( * ) SI_UNIT ( $, .STERADIAN. ) SOLID_ANGLE_UNIT ( ) );
#6967=VECTOR ( 'NONE', #3192, 39.37007874015748143 ) ;
#7021=CARTESIAN_POINT ( 'NONE',  ( 1.220472440944881942, 0.7480314960629921295, 0.000000000000000000 ) ) ;
#7024=DIRECTION ( 'NONE',  ( 0.000000000000000000, 0.000000000000000000, 1.000000000000000000 ) ) ;
#7053=CYLINDRICAL_SURFACE ( 'NONE', #5914, 0.2362204724409449341 ) ;
#7098=CARTESIAN_POINT ( 'NONE',  ( 0.000000000000000000, 1.496062992125984259, 0.000000000000000000 ) ) ;
#7117=VECTOR ( 'NONE', #5311, 39.37007874015748143 ) ;
#7129=SHAPE_REPRESENTATION_RELATIONSHIP ( 'NONE' , 'NONE' ,  #5531, #6873 ) ;
#7130=AXIS2_PLACEMENT_3D ( 'NONE', #7098, #64, #4810 ) ;
#7136=DIRECTION ( 'NONE',  ( 0.000000000000000000, 0.000000000000000000, 1.000000000000000000 ) ) ;
#7146=DIRECTION ( 'NONE',  ( 0.000000000000000000, 0.000000000000000000, -1.000000000000000000 ) ) ;
#7153=VERTEX_POINT ( 'NONE', #5172 ) ;
#7187=ORIENTED_EDGE ( 'NONE', *, *, #5808, .F. ) ;
#7245=EDGE_CURVE ( 'NONE', #7450, #7153, #7511, .T. ) ;
#7258=ORIENTED_EDGE ( 'NONE', *, *, #3280, .T. ) ;
#7300=DIRECTION ( 'NONE',  ( 1.000000000000000000, 0.000000000000000000, -0.000000000000000000 ) ) ;
#7309=ORIENTED_EDGE ( 'NONE', *, *, #2879, .F. ) ;
#7312=AXIS2_PLACEMENT_3D ( 'NONE', #3062, #5324, #4795 ) ;
#7322=CARTESIAN_POINT ( 'NONE',  ( 0.000000000000000000, 0.000000000000000000, -0.2362204724409449341 ) ) ;
#7337=ORIENTED_EDGE ( 'NONE', *, *, #6639, .F. ) ;
#7338=AXIS2_PLACEMENT_3D ( 'NONE', #5976, #167, #7146 ) ;
#7347=DIRECTION ( 'NONE',  ( -0.000000000000000000, -0.000000000000000000, 1.000000000000000000 ) ) ;
#7379=DIRECTION ( 'NONE',  ( -0.000000000000000000, -1.000000000000000000, -0.000000000000000000 ) ) ;
#7381=( NAMED_UNIT ( * ) SI_UNIT ( $, .STERADIAN. ) SOLID_ANGLE_UNIT ( ) );
#7382=EDGE_LOOP ( 'NONE', ( #4209, #21, #1573, #2553 ) ) ;
#7387=EDGE_CURVE ( 'NONE', #4527, #3346, #6127, .T. ) ;
#7450=VERTEX_POINT ( 'NONE', #5508 ) ;
#7455=( NAMED_UNIT ( * ) PLANE_ANGLE_UNIT ( ) SI_UNIT ( $, .RADIAN. ) );
#7458=ORIENTED_EDGE ( 'NONE', *, *, #4398, .T. ) ;
#7511=LINE ( 'NONE', #4587, #627 ) ;
#7567=COLOUR_RGB('Sky Blue',0.24,0.69,0.87);
#7568=FILL_AREA_STYLE_COLOUR('',#7567);
#7569=FILL_AREA_STYLE('',(#7568));
#7570=SURFACE_STYLE_FILL_AREA(#7569);
#7571=SURFACE_SIDE_STYLE('',(#7570));
#7572=SURFACE_STYLE_USAGE(.BOTH.,#7571);
#7573=PRESENTATION_STYLE_ASSIGNMENT((#7572));
ENDSEC;
END-ISO-10303-21;
